ISO-10303-21;
HEADER;
/* Generated by software containing ST-Developer
 * from STEP Tools, Inc. (www.steptools.com) 
 */

FILE_DESCRIPTION(
/* description */ ('Bin tilter linkage'),
/* implementation_level */ '2;1');

FILE_NAME(
/* name */ 'Pivot post (1).step',
/* time_stamp */ '2026-10-28T03:26:24-07:00',
/* author */ (''),
/* organization */ (''),
/* preprocessor_version */ 'ST-DEVELOPER v20.2',
/* originating_system */ 'Autodesk Translation Framework v15.17.0.0',
/* authorisation */ '');

FILE_SCHEMA (('AUTOMOTIVE_DESIGN { 1 0 10303 214 3 1 1 }'));
ENDSEC;

DATA;
#10=MECHANICAL_DESIGN_GEOMETRIC_PRESENTATION_REPRESENTATION('',(#866),#23728);
#654=SHAPE_REPRESENTATION_RELATIONSHIP('SRR','None',#24118,#760);
#760=ADVANCED_BREP_SHAPE_REPRESENTATION('',(#980),#23618);
#866=STYLED_ITEM('',(#24779),#980);
#980=MANIFOLD_SOLID_BREP('Body1',#12396);
#1127=FACE_BOUND('',#2764,.T.);
#1128=FACE_BOUND('',#2765,.T.);
#1129=FACE_BOUND('',#2766,.T.);
#1130=FACE_BOUND('',#2767,.T.);
#1131=FACE_BOUND('',#2772,.T.);
#1132=FACE_BOUND('',#2773,.T.);
#1133=FACE_BOUND('',#2774,.T.);
#1134=FACE_BOUND('',#2775,.T.);
#1135=FACE_BOUND('',#2778,.T.);
#1136=FACE_BOUND('',#2779,.T.);
#1137=FACE_BOUND('',#2780,.T.);
#1138=FACE_BOUND('',#2781,.T.);
#1139=FACE_BOUND('',#2785,.T.);
#1140=FACE_BOUND('',#2786,.T.);
#1141=FACE_BOUND('',#2787,.T.);
#1142=FACE_BOUND('',#2788,.T.);
#1520=PLANE('',#13795);
#1521=PLANE('',#13796);
#1522=PLANE('',#13797);
#1523=PLANE('',#13798);
#1524=PLANE('',#13799);
#1525=PLANE('',#13800);
#1526=PLANE('',#13801);
#1527=PLANE('',#13802);
#1528=PLANE('',#13803);
#1529=PLANE('',#13804);
#1938=FACE_OUTER_BOUND('',#2755,.T.);
#1939=FACE_OUTER_BOUND('',#2756,.T.);
#1940=FACE_OUTER_BOUND('',#2757,.T.);
#1941=FACE_OUTER_BOUND('',#2758,.T.);
#1942=FACE_OUTER_BOUND('',#2759,.T.);
#1943=FACE_OUTER_BOUND('',#2760,.T.);
#1944=FACE_OUTER_BOUND('',#2761,.T.);
#1945=FACE_OUTER_BOUND('',#2762,.T.);
#1946=FACE_OUTER_BOUND('',#2763,.T.);
#1947=FACE_OUTER_BOUND('',#2768,.T.);
#1948=FACE_OUTER_BOUND('',#2769,.T.);
#1949=FACE_OUTER_BOUND('',#2770,.T.);
#1950=FACE_OUTER_BOUND('',#2771,.T.);
#1951=FACE_OUTER_BOUND('',#2776,.T.);
#1952=FACE_OUTER_BOUND('',#2777,.T.);
#1953=FACE_OUTER_BOUND('',#2782,.T.);
#1954=FACE_OUTER_BOUND('',#2783,.T.);
#1955=FACE_OUTER_BOUND('',#2784,.T.);
#2755=EDGE_LOOP('',(#8613,#8614,#8615,#8616));
#2756=EDGE_LOOP('',(#8617,#8618,#8619,#8620));
#2757=EDGE_LOOP('',(#8621,#8622,#8623,#8624));
#2758=EDGE_LOOP('',(#8625,#8626,#8627,#8628));
#2759=EDGE_LOOP('',(#8629,#8630,#8631,#8632));
#2760=EDGE_LOOP('',(#8633,#8634,#8635,#8636));
#2761=EDGE_LOOP('',(#8637,#8638,#8639,#8640));
#2762=EDGE_LOOP('',(#8641,#8642,#8643,#8644));
#2763=EDGE_LOOP('',(#8645,#8646,#8647,#8648,#8649,#8650,#8651,#8652));
#2764=EDGE_LOOP('',(#8653));
#2765=EDGE_LOOP('',(#8654));
#2766=EDGE_LOOP('',(#8655));
#2767=EDGE_LOOP('',(#8656));
#2768=EDGE_LOOP('',(#8657,#8658,#8659,#8660));
#2769=EDGE_LOOP('',(#8661,#8662,#8663,#8664));
#2770=EDGE_LOOP('',(#8665,#8666,#8667,#8668));
#2771=EDGE_LOOP('',(#8669,#8670,#8671,#8672,#8673,#8674,#8675,#8676));
#2772=EDGE_LOOP('',(#8677));
#2773=EDGE_LOOP('',(#8678));
#2774=EDGE_LOOP('',(#8679));
#2775=EDGE_LOOP('',(#8680));
#2776=EDGE_LOOP('',(#8681,#8682,#8683,#8684));
#2777=EDGE_LOOP('',(#8685,#8686,#8687,#8688));
#2778=EDGE_LOOP('',(#8689));
#2779=EDGE_LOOP('',(#8690));
#2780=EDGE_LOOP('',(#8691));
#2781=EDGE_LOOP('',(#8692));
#2782=EDGE_LOOP('',(#8693,#8694,#8695,#8696));
#2783=EDGE_LOOP('',(#8697,#8698,#8699,#8700));
#2784=EDGE_LOOP('',(#8701,#8702,#8703,#8704));
#2785=EDGE_LOOP('',(#8705));
#2786=EDGE_LOOP('',(#8706));
#2787=EDGE_LOOP('',(#8707));
#2788=EDGE_LOOP('',(#8708));
#3929=LINE('',#20004,#4604);
#3930=LINE('',#20010,#4605);
#3931=LINE('',#20016,#4606);
#3932=LINE('',#20022,#4607);
#3933=LINE('',#20028,#4608);
#3934=LINE('',#20034,#4609);
#3935=LINE('',#20040,#4610);
#3936=LINE('',#20046,#4611);
#3937=LINE('',#20051,#4612);
#3938=LINE('',#20053,#4613);
#3939=LINE('',#20055,#4614);
#3940=LINE('',#20057,#4615);
#3941=LINE('',#20059,#4616);
#3942=LINE('',#20061,#4617);
#3943=LINE('',#20063,#4618);
#3944=LINE('',#20064,#4619);
#3945=LINE('',#20067,#4620);
#3946=LINE('',#20069,#4621);
#3947=LINE('',#20070,#4622);
#3948=LINE('',#20073,#4623);
#3949=LINE('',#20075,#4624);
#3950=LINE('',#20076,#4625);
#3951=LINE('',#20078,#4626);
#3952=LINE('',#20081,#4627);
#3953=LINE('',#20083,#4628);
#3954=LINE('',#20084,#4629);
#3955=LINE('',#20085,#4630);
#3956=LINE('',#20088,#4631);
#3957=LINE('',#20089,#4632);
#3958=LINE('',#20092,#4633);
#3959=LINE('',#20093,#4634);
#3960=LINE('',#20095,#4635);
#4604=VECTOR('',#15748,0.164999999999999);
#4605=VECTOR('',#15755,0.164999999999999);
#4606=VECTOR('',#15762,0.164999999999999);
#4607=VECTOR('',#15769,0.605);
#4608=VECTOR('',#15776,0.274999999999999);
#4609=VECTOR('',#15783,0.274999999999999);
#4610=VECTOR('',#15790,0.275);
#4611=VECTOR('',#15797,0.275);
#4612=VECTOR('',#15802,1.);
#4613=VECTOR('',#15803,1.);
#4614=VECTOR('',#15804,1.);
#4615=VECTOR('',#15805,1.);
#4616=VECTOR('',#15806,1.);
#4617=VECTOR('',#15807,1.);
#4618=VECTOR('',#15808,1.);
#4619=VECTOR('',#15809,1.);
#4620=VECTOR('',#15812,1.);
#4621=VECTOR('',#15813,1.);
#4622=VECTOR('',#15814,1.);
#4623=VECTOR('',#15817,1.);
#4624=VECTOR('',#15818,1.);
#4625=VECTOR('',#15819,1.);
#4626=VECTOR('',#15822,1.);
#4627=VECTOR('',#15825,1.);
#4628=VECTOR('',#15826,1.);
#4629=VECTOR('',#15827,1.);
#4630=VECTOR('',#15828,1.);
#4631=VECTOR('',#15831,1.);
#4632=VECTOR('',#15832,1.);
#4633=VECTOR('',#15835,1.);
#4634=VECTOR('',#15836,1.);
#4635=VECTOR('',#15839,1.);
#5239=CIRCLE('',#13772,0.164999999999999);
#5240=CIRCLE('',#13773,0.164999999999999);
#5241=CIRCLE('',#13775,0.164999999999999);
#5242=CIRCLE('',#13776,0.164999999999999);
#5243=CIRCLE('',#13778,0.164999999999999);
#5244=CIRCLE('',#13779,0.164999999999999);
#5245=CIRCLE('',#13781,0.605);
#5246=CIRCLE('',#13782,0.605);
#5247=CIRCLE('',#13784,0.274999999999999);
#5248=CIRCLE('',#13785,0.274999999999999);
#5249=CIRCLE('',#13787,0.274999999999999);
#5250=CIRCLE('',#13788,0.274999999999999);
#5251=CIRCLE('',#13790,0.275);
#5252=CIRCLE('',#13791,0.275);
#5253=CIRCLE('',#13793,0.275);
#5254=CIRCLE('',#13794,0.275);
#6037=VERTEX_POINT('',#20001);
#6038=VERTEX_POINT('',#20003);
#6039=VERTEX_POINT('',#20007);
#6040=VERTEX_POINT('',#20009);
#6041=VERTEX_POINT('',#20013);
#6042=VERTEX_POINT('',#20015);
#6043=VERTEX_POINT('',#20019);
#6044=VERTEX_POINT('',#20021);
#6045=VERTEX_POINT('',#20025);
#6046=VERTEX_POINT('',#20027);
#6047=VERTEX_POINT('',#20031);
#6048=VERTEX_POINT('',#20033);
#6049=VERTEX_POINT('',#20037);
#6050=VERTEX_POINT('',#20039);
#6051=VERTEX_POINT('',#20043);
#6052=VERTEX_POINT('',#20045);
#6053=VERTEX_POINT('',#20049);
#6054=VERTEX_POINT('',#20050);
#6055=VERTEX_POINT('',#20052);
#6056=VERTEX_POINT('',#20054);
#6057=VERTEX_POINT('',#20056);
#6058=VERTEX_POINT('',#20058);
#6059=VERTEX_POINT('',#20060);
#6060=VERTEX_POINT('',#20062);
#6061=VERTEX_POINT('',#20066);
#6062=VERTEX_POINT('',#20068);
#6063=VERTEX_POINT('',#20072);
#6064=VERTEX_POINT('',#20074);
#6065=VERTEX_POINT('',#20080);
#6066=VERTEX_POINT('',#20082);
#6067=VERTEX_POINT('',#20087);
#6068=VERTEX_POINT('',#20091);
#7046=EDGE_CURVE('',#6037,#6037,#5239,.T.);
#7047=EDGE_CURVE('',#6037,#6038,#3929,.T.);
#7048=EDGE_CURVE('',#6038,#6038,#5240,.T.);
#7049=EDGE_CURVE('',#6039,#6039,#5241,.T.);
#7050=EDGE_CURVE('',#6039,#6040,#3930,.T.);
#7051=EDGE_CURVE('',#6040,#6040,#5242,.T.);
#7052=EDGE_CURVE('',#6041,#6041,#5243,.T.);
#7053=EDGE_CURVE('',#6041,#6042,#3931,.T.);
#7054=EDGE_CURVE('',#6042,#6042,#5244,.T.);
#7055=EDGE_CURVE('',#6043,#6043,#5245,.T.);
#7056=EDGE_CURVE('',#6043,#6044,#3932,.T.);
#7057=EDGE_CURVE('',#6044,#6044,#5246,.T.);
#7058=EDGE_CURVE('',#6045,#6045,#5247,.T.);
#7059=EDGE_CURVE('',#6045,#6046,#3933,.T.);
#7060=EDGE_CURVE('',#6046,#6046,#5248,.T.);
#7061=EDGE_CURVE('',#6047,#6047,#5249,.T.);
#7062=EDGE_CURVE('',#6047,#6048,#3934,.T.);
#7063=EDGE_CURVE('',#6048,#6048,#5250,.T.);
#7064=EDGE_CURVE('',#6049,#6049,#5251,.T.);
#7065=EDGE_CURVE('',#6049,#6050,#3935,.T.);
#7066=EDGE_CURVE('',#6050,#6050,#5252,.T.);
#7067=EDGE_CURVE('',#6051,#6051,#5253,.T.);
#7068=EDGE_CURVE('',#6051,#6052,#3936,.T.);
#7069=EDGE_CURVE('',#6052,#6052,#5254,.T.);
#7070=EDGE_CURVE('',#6053,#6054,#3937,.T.);
#7071=EDGE_CURVE('',#6055,#6053,#3938,.T.);
#7072=EDGE_CURVE('',#6056,#6055,#3939,.T.);
#7073=EDGE_CURVE('',#6057,#6056,#3940,.T.);
#7074=EDGE_CURVE('',#6057,#6058,#3941,.T.);
#7075=EDGE_CURVE('',#6059,#6058,#3942,.T.);
#7076=EDGE_CURVE('',#6060,#6059,#3943,.T.);
#7077=EDGE_CURVE('',#6054,#6060,#3944,.T.);
#7078=EDGE_CURVE('',#6060,#6061,#3945,.T.);
#7079=EDGE_CURVE('',#6062,#6059,#3946,.T.);
#7080=EDGE_CURVE('',#6061,#6062,#3947,.T.);
#7081=EDGE_CURVE('',#6063,#6057,#3948,.T.);
#7082=EDGE_CURVE('',#6063,#6064,#3949,.T.);
#7083=EDGE_CURVE('',#6058,#6064,#3950,.T.);
#7084=EDGE_CURVE('',#6064,#6062,#3951,.T.);
#7085=EDGE_CURVE('',#6056,#6065,#3952,.T.);
#7086=EDGE_CURVE('',#6066,#6065,#3953,.T.);
#7087=EDGE_CURVE('',#6054,#6066,#3954,.T.);
#7088=EDGE_CURVE('',#6061,#6063,#3955,.T.);
#7089=EDGE_CURVE('',#6055,#6067,#3956,.T.);
#7090=EDGE_CURVE('',#6065,#6067,#3957,.T.);
#7091=EDGE_CURVE('',#6053,#6068,#3958,.T.);
#7092=EDGE_CURVE('',#6067,#6068,#3959,.T.);
#7093=EDGE_CURVE('',#6068,#6066,#3960,.T.);
#8613=ORIENTED_EDGE('',*,*,#7046,.F.);
#8614=ORIENTED_EDGE('',*,*,#7047,.T.);
#8615=ORIENTED_EDGE('',*,*,#7048,.F.);
#8616=ORIENTED_EDGE('',*,*,#7047,.F.);
#8617=ORIENTED_EDGE('',*,*,#7049,.F.);
#8618=ORIENTED_EDGE('',*,*,#7050,.T.);
#8619=ORIENTED_EDGE('',*,*,#7051,.F.);
#8620=ORIENTED_EDGE('',*,*,#7050,.F.);
#8621=ORIENTED_EDGE('',*,*,#7052,.F.);
#8622=ORIENTED_EDGE('',*,*,#7053,.T.);
#8623=ORIENTED_EDGE('',*,*,#7054,.F.);
#8624=ORIENTED_EDGE('',*,*,#7053,.F.);
#8625=ORIENTED_EDGE('',*,*,#7055,.F.);
#8626=ORIENTED_EDGE('',*,*,#7056,.T.);
#8627=ORIENTED_EDGE('',*,*,#7057,.F.);
#8628=ORIENTED_EDGE('',*,*,#7056,.F.);
#8629=ORIENTED_EDGE('',*,*,#7058,.F.);
#8630=ORIENTED_EDGE('',*,*,#7059,.T.);
#8631=ORIENTED_EDGE('',*,*,#7060,.F.);
#8632=ORIENTED_EDGE('',*,*,#7059,.F.);
#8633=ORIENTED_EDGE('',*,*,#7061,.F.);
#8634=ORIENTED_EDGE('',*,*,#7062,.T.);
#8635=ORIENTED_EDGE('',*,*,#7063,.F.);
#8636=ORIENTED_EDGE('',*,*,#7062,.F.);
#8637=ORIENTED_EDGE('',*,*,#7064,.F.);
#8638=ORIENTED_EDGE('',*,*,#7065,.T.);
#8639=ORIENTED_EDGE('',*,*,#7066,.F.);
#8640=ORIENTED_EDGE('',*,*,#7065,.F.);
#8641=ORIENTED_EDGE('',*,*,#7067,.F.);
#8642=ORIENTED_EDGE('',*,*,#7068,.T.);
#8643=ORIENTED_EDGE('',*,*,#7069,.F.);
#8644=ORIENTED_EDGE('',*,*,#7068,.F.);
#8645=ORIENTED_EDGE('',*,*,#7070,.F.);
#8646=ORIENTED_EDGE('',*,*,#7071,.F.);
#8647=ORIENTED_EDGE('',*,*,#7072,.F.);
#8648=ORIENTED_EDGE('',*,*,#7073,.F.);
#8649=ORIENTED_EDGE('',*,*,#7074,.T.);
#8650=ORIENTED_EDGE('',*,*,#7075,.F.);
#8651=ORIENTED_EDGE('',*,*,#7076,.F.);
#8652=ORIENTED_EDGE('',*,*,#7077,.F.);
#8653=ORIENTED_EDGE('',*,*,#7060,.T.);
#8654=ORIENTED_EDGE('',*,*,#7063,.T.);
#8655=ORIENTED_EDGE('',*,*,#7066,.T.);
#8656=ORIENTED_EDGE('',*,*,#7069,.T.);
#8657=ORIENTED_EDGE('',*,*,#7078,.F.);
#8658=ORIENTED_EDGE('',*,*,#7076,.T.);
#8659=ORIENTED_EDGE('',*,*,#7079,.F.);
#8660=ORIENTED_EDGE('',*,*,#7080,.F.);
#8661=ORIENTED_EDGE('',*,*,#7081,.F.);
#8662=ORIENTED_EDGE('',*,*,#7082,.T.);
#8663=ORIENTED_EDGE('',*,*,#7083,.F.);
#8664=ORIENTED_EDGE('',*,*,#7074,.F.);
#8665=ORIENTED_EDGE('',*,*,#7075,.T.);
#8666=ORIENTED_EDGE('',*,*,#7083,.T.);
#8667=ORIENTED_EDGE('',*,*,#7084,.T.);
#8668=ORIENTED_EDGE('',*,*,#7079,.T.);
#8669=ORIENTED_EDGE('',*,*,#7085,.T.);
#8670=ORIENTED_EDGE('',*,*,#7086,.F.);
#8671=ORIENTED_EDGE('',*,*,#7087,.F.);
#8672=ORIENTED_EDGE('',*,*,#7077,.T.);
#8673=ORIENTED_EDGE('',*,*,#7078,.T.);
#8674=ORIENTED_EDGE('',*,*,#7088,.T.);
#8675=ORIENTED_EDGE('',*,*,#7081,.T.);
#8676=ORIENTED_EDGE('',*,*,#7073,.T.);
#8677=ORIENTED_EDGE('',*,*,#7046,.T.);
#8678=ORIENTED_EDGE('',*,*,#7049,.T.);
#8679=ORIENTED_EDGE('',*,*,#7052,.T.);
#8680=ORIENTED_EDGE('',*,*,#7055,.T.);
#8681=ORIENTED_EDGE('',*,*,#7072,.T.);
#8682=ORIENTED_EDGE('',*,*,#7089,.T.);
#8683=ORIENTED_EDGE('',*,*,#7090,.F.);
#8684=ORIENTED_EDGE('',*,*,#7085,.F.);
#8685=ORIENTED_EDGE('',*,*,#7071,.T.);
#8686=ORIENTED_EDGE('',*,*,#7091,.T.);
#8687=ORIENTED_EDGE('',*,*,#7092,.F.);
#8688=ORIENTED_EDGE('',*,*,#7089,.F.);
#8689=ORIENTED_EDGE('',*,*,#7048,.T.);
#8690=ORIENTED_EDGE('',*,*,#7051,.T.);
#8691=ORIENTED_EDGE('',*,*,#7054,.T.);
#8692=ORIENTED_EDGE('',*,*,#7057,.T.);
#8693=ORIENTED_EDGE('',*,*,#7070,.T.);
#8694=ORIENTED_EDGE('',*,*,#7087,.T.);
#8695=ORIENTED_EDGE('',*,*,#7093,.F.);
#8696=ORIENTED_EDGE('',*,*,#7091,.F.);
#8697=ORIENTED_EDGE('',*,*,#7093,.T.);
#8698=ORIENTED_EDGE('',*,*,#7086,.T.);
#8699=ORIENTED_EDGE('',*,*,#7090,.T.);
#8700=ORIENTED_EDGE('',*,*,#7092,.T.);
#8701=ORIENTED_EDGE('',*,*,#7088,.F.);
#8702=ORIENTED_EDGE('',*,*,#7080,.T.);
#8703=ORIENTED_EDGE('',*,*,#7084,.F.);
#8704=ORIENTED_EDGE('',*,*,#7082,.F.);
#8705=ORIENTED_EDGE('',*,*,#7058,.T.);
#8706=ORIENTED_EDGE('',*,*,#7061,.T.);
#8707=ORIENTED_EDGE('',*,*,#7064,.T.);
#8708=ORIENTED_EDGE('',*,*,#7067,.T.);
#11287=CYLINDRICAL_SURFACE('',#13771,0.164999999999999);
#11288=CYLINDRICAL_SURFACE('',#13774,0.164999999999999);
#11289=CYLINDRICAL_SURFACE('',#13777,0.164999999999999);
#11290=CYLINDRICAL_SURFACE('',#13780,0.605);
#11291=CYLINDRICAL_SURFACE('',#13783,0.274999999999999);
#11292=CYLINDRICAL_SURFACE('',#13786,0.274999999999999);
#11293=CYLINDRICAL_SURFACE('',#13789,0.275);
#11294=CYLINDRICAL_SURFACE('',#13792,0.275);
#11663=ADVANCED_FACE('',(#1938),#11287,.F.);
#11664=ADVANCED_FACE('',(#1939),#11288,.F.);
#11665=ADVANCED_FACE('',(#1940),#11289,.F.);
#11666=ADVANCED_FACE('',(#1941),#11290,.F.);
#11667=ADVANCED_FACE('',(#1942),#11291,.F.);
#11668=ADVANCED_FACE('',(#1943),#11292,.F.);
#11669=ADVANCED_FACE('',(#1944),#11293,.F.);
#11670=ADVANCED_FACE('',(#1945),#11294,.F.);
#11671=ADVANCED_FACE('',(#1946,#1127,#1128,#1129,#1130),#1520,.T.);
#11672=ADVANCED_FACE('',(#1947),#1521,.T.);
#11673=ADVANCED_FACE('',(#1948),#1522,.T.);
#11674=ADVANCED_FACE('',(#1949),#1523,.T.);
#11675=ADVANCED_FACE('',(#1950,#1131,#1132,#1133,#1134),#1524,.T.);
#11676=ADVANCED_FACE('',(#1951),#1525,.T.);
#11677=ADVANCED_FACE('',(#1952,#1135,#1136,#1137,#1138),#1526,.T.);
#11678=ADVANCED_FACE('',(#1953),#1527,.T.);
#11679=ADVANCED_FACE('',(#1954),#1528,.T.);
#11680=ADVANCED_FACE('',(#1955,#1139,#1140,#1141,#1142),#1529,.F.);
#12396=CLOSED_SHELL('',(#11663,#11664,#11665,#11666,#11667,#11668,#11669,
#11670,#11671,#11672,#11673,#11674,#11675,#11676,#11677,#11678,#11679,#11680));
#13770=AXIS2_PLACEMENT_3D('',#19999,#15742,#15743);
#13771=AXIS2_PLACEMENT_3D('',#20000,#15744,#15745);
#13772=AXIS2_PLACEMENT_3D('',#20002,#15746,#15747);
#13773=AXIS2_PLACEMENT_3D('',#20005,#15749,#15750);
#13774=AXIS2_PLACEMENT_3D('',#20006,#15751,#15752);
#13775=AXIS2_PLACEMENT_3D('',#20008,#15753,#15754);
#13776=AXIS2_PLACEMENT_3D('',#20011,#15756,#15757);
#13777=AXIS2_PLACEMENT_3D('',#20012,#15758,#15759);
#13778=AXIS2_PLACEMENT_3D('',#20014,#15760,#15761);
#13779=AXIS2_PLACEMENT_3D('',#20017,#15763,#15764);
#13780=AXIS2_PLACEMENT_3D('',#20018,#15765,#15766);
#13781=AXIS2_PLACEMENT_3D('',#20020,#15767,#15768);
#13782=AXIS2_PLACEMENT_3D('',#20023,#15770,#15771);
#13783=AXIS2_PLACEMENT_3D('',#20024,#15772,#15773);
#13784=AXIS2_PLACEMENT_3D('',#20026,#15774,#15775);
#13785=AXIS2_PLACEMENT_3D('',#20029,#15777,#15778);
#13786=AXIS2_PLACEMENT_3D('',#20030,#15779,#15780);
#13787=AXIS2_PLACEMENT_3D('',#20032,#15781,#15782);
#13788=AXIS2_PLACEMENT_3D('',#20035,#15784,#15785);
#13789=AXIS2_PLACEMENT_3D('',#20036,#15786,#15787);
#13790=AXIS2_PLACEMENT_3D('',#20038,#15788,#15789);
#13791=AXIS2_PLACEMENT_3D('',#20041,#15791,#15792);
#13792=AXIS2_PLACEMENT_3D('',#20042,#15793,#15794);
#13793=AXIS2_PLACEMENT_3D('',#20044,#15795,#15796);
#13794=AXIS2_PLACEMENT_3D('',#20047,#15798,#15799);
#13795=AXIS2_PLACEMENT_3D('',#20048,#15800,#15801);
#13796=AXIS2_PLACEMENT_3D('',#20065,#15810,#15811);
#13797=AXIS2_PLACEMENT_3D('',#20071,#15815,#15816);
#13798=AXIS2_PLACEMENT_3D('',#20077,#15820,#15821);
#13799=AXIS2_PLACEMENT_3D('',#20079,#15823,#15824);
#13800=AXIS2_PLACEMENT_3D('',#20086,#15829,#15830);
#13801=AXIS2_PLACEMENT_3D('',#20090,#15833,#15834);
#13802=AXIS2_PLACEMENT_3D('',#20094,#15837,#15838);
#13803=AXIS2_PLACEMENT_3D('',#20096,#15840,#15841);
#13804=AXIS2_PLACEMENT_3D('',#20097,#15842,#15843);
#15742=DIRECTION('axis',(0.,0.,1.));
#15743=DIRECTION('refdir',(1.,0.,0.));
#15744=DIRECTION('center_axis',(0.,1.,0.));
#15745=DIRECTION('ref_axis',(1.,0.,0.));
#15746=DIRECTION('center_axis',(0.,1.,0.));
#15747=DIRECTION('ref_axis',(1.,0.,0.));
#15748=DIRECTION('',(0.,1.,0.));
#15749=DIRECTION('center_axis',(0.,-1.,0.));
#15750=DIRECTION('ref_axis',(1.,0.,0.));
#15751=DIRECTION('center_axis',(0.,1.,0.));
#15752=DIRECTION('ref_axis',(1.,0.,0.));
#15753=DIRECTION('center_axis',(0.,1.,0.));
#15754=DIRECTION('ref_axis',(1.,0.,0.));
#15755=DIRECTION('',(0.,1.,0.));
#15756=DIRECTION('center_axis',(0.,-1.,0.));
#15757=DIRECTION('ref_axis',(1.,0.,0.));
#15758=DIRECTION('center_axis',(0.,1.,0.));
#15759=DIRECTION('ref_axis',(1.,0.,0.));
#15760=DIRECTION('center_axis',(0.,1.,0.));
#15761=DIRECTION('ref_axis',(1.,0.,0.));
#15762=DIRECTION('',(0.,1.,0.));
#15763=DIRECTION('center_axis',(0.,-1.,0.));
#15764=DIRECTION('ref_axis',(1.,0.,0.));
#15765=DIRECTION('center_axis',(0.,1.,0.));
#15766=DIRECTION('ref_axis',(1.,0.,0.));
#15767=DIRECTION('center_axis',(0.,1.,0.));
#15768=DIRECTION('ref_axis',(1.,0.,0.));
#15769=DIRECTION('',(0.,1.,0.));
#15770=DIRECTION('center_axis',(0.,-1.,0.));
#15771=DIRECTION('ref_axis',(1.,0.,0.));
#15772=DIRECTION('center_axis',(0.,0.,1.));
#15773=DIRECTION('ref_axis',(1.,0.,0.));
#15774=DIRECTION('center_axis',(0.,0.,1.));
#15775=DIRECTION('ref_axis',(1.,0.,0.));
#15776=DIRECTION('',(0.,0.,1.));
#15777=DIRECTION('center_axis',(0.,0.,-1.));
#15778=DIRECTION('ref_axis',(1.,0.,0.));
#15779=DIRECTION('center_axis',(0.,0.,1.));
#15780=DIRECTION('ref_axis',(1.,0.,0.));
#15781=DIRECTION('center_axis',(0.,0.,1.));
#15782=DIRECTION('ref_axis',(1.,0.,0.));
#15783=DIRECTION('',(0.,0.,1.));
#15784=DIRECTION('center_axis',(0.,0.,-1.));
#15785=DIRECTION('ref_axis',(1.,0.,0.));
#15786=DIRECTION('center_axis',(0.,0.,1.));
#15787=DIRECTION('ref_axis',(1.,0.,0.));
#15788=DIRECTION('center_axis',(0.,0.,1.));
#15789=DIRECTION('ref_axis',(1.,0.,0.));
#15790=DIRECTION('',(0.,0.,1.));
#15791=DIRECTION('center_axis',(0.,0.,-1.));
#15792=DIRECTION('ref_axis',(1.,0.,0.));
#15793=DIRECTION('center_axis',(0.,0.,1.));
#15794=DIRECTION('ref_axis',(1.,0.,0.));
#15795=DIRECTION('center_axis',(0.,0.,1.));
#15796=DIRECTION('ref_axis',(1.,0.,0.));
#15797=DIRECTION('',(0.,0.,1.));
#15798=DIRECTION('center_axis',(0.,0.,-1.));
#15799=DIRECTION('ref_axis',(1.,0.,0.));
#15800=DIRECTION('center_axis',(0.,0.,1.));
#15801=DIRECTION('ref_axis',(1.,0.,0.));
#15802=DIRECTION('',(0.,-1.,0.));
#15803=DIRECTION('',(-1.,0.,0.));
#15804=DIRECTION('',(0.,1.,0.));
#15805=DIRECTION('',(-1.,0.,0.));
#15806=DIRECTION('',(0.,1.,0.));
#15807=DIRECTION('',(1.,0.,0.));
#15808=DIRECTION('',(0.,1.,0.));
#15809=DIRECTION('',(-1.,0.,0.));
#15810=DIRECTION('center_axis',(-1.,0.,0.));
#15811=DIRECTION('ref_axis',(0.,0.,1.));
#15812=DIRECTION('',(0.,0.,-1.));
#15813=DIRECTION('',(0.,0.,1.));
#15814=DIRECTION('',(0.,1.,0.));
#15815=DIRECTION('center_axis',(1.,0.,0.));
#15816=DIRECTION('ref_axis',(0.,0.,-1.));
#15817=DIRECTION('',(0.,0.,1.));
#15818=DIRECTION('',(0.,1.,0.));
#15819=DIRECTION('',(0.,0.,-1.));
#15820=DIRECTION('center_axis',(0.,1.,0.));
#15821=DIRECTION('ref_axis',(0.,0.,1.));
#15822=DIRECTION('',(-1.,0.,0.));
#15823=DIRECTION('center_axis',(0.,-1.,0.));
#15824=DIRECTION('ref_axis',(1.,0.,0.));
#15825=DIRECTION('',(0.,0.,1.));
#15826=DIRECTION('',(1.,0.,0.));
#15827=DIRECTION('',(0.,0.,1.));
#15828=DIRECTION('',(1.,0.,0.));
#15829=DIRECTION('center_axis',(1.,0.,0.));
#15830=DIRECTION('ref_axis',(0.,1.,0.));
#15831=DIRECTION('',(0.,0.,1.));
#15832=DIRECTION('',(0.,1.,0.));
#15833=DIRECTION('center_axis',(0.,1.,0.));
#15834=DIRECTION('ref_axis',(-1.,0.,0.));
#15835=DIRECTION('',(0.,0.,1.));
#15836=DIRECTION('',(-1.,0.,0.));
#15837=DIRECTION('center_axis',(-1.,0.,0.));
#15838=DIRECTION('ref_axis',(0.,-1.,0.));
#15839=DIRECTION('',(0.,-1.,0.));
#15840=DIRECTION('center_axis',(0.,0.,1.));
#15841=DIRECTION('ref_axis',(1.,0.,0.));
#15842=DIRECTION('center_axis',(0.,0.,1.));
#15843=DIRECTION('ref_axis',(1.,0.,0.));
#19999=CARTESIAN_POINT('',(0.,0.,0.));
#20000=CARTESIAN_POINT('Origin',(19.15,4.4,15.));
#20001=CARTESIAN_POINT('',(18.985,4.5,15.));
#20002=CARTESIAN_POINT('Origin',(19.15,4.5,15.));
#20003=CARTESIAN_POINT('',(18.985,5.5,15.));
#20004=CARTESIAN_POINT('',(18.985,4.4,15.));
#20005=CARTESIAN_POINT('Origin',(19.15,5.5,15.));
#20006=CARTESIAN_POINT('Origin',(17.425,4.4,15.9959292143521));
#20007=CARTESIAN_POINT('',(17.26,4.5,15.9959292143521));
#20008=CARTESIAN_POINT('Origin',(17.425,4.5,15.9959292143521));
#20009=CARTESIAN_POINT('',(17.26,5.5,15.9959292143521));
#20010=CARTESIAN_POINT('',(17.26,4.4,15.9959292143521));
#20011=CARTESIAN_POINT('Origin',(17.425,5.5,15.9959292143521));
#20012=CARTESIAN_POINT('Origin',(17.425,4.4,14.0040707856479));
#20013=CARTESIAN_POINT('',(17.26,4.5,14.0040707856479));
#20014=CARTESIAN_POINT('Origin',(17.425,4.5,14.0040707856479));
#20015=CARTESIAN_POINT('',(17.26,5.5,14.0040707856479));
#20016=CARTESIAN_POINT('',(17.26,4.4,14.0040707856479));
#20017=CARTESIAN_POINT('Origin',(17.425,5.5,14.0040707856479));
#20018=CARTESIAN_POINT('Origin',(18.,4.4,15.));
#20019=CARTESIAN_POINT('',(17.395,4.5,15.));
#20020=CARTESIAN_POINT('Origin',(18.,4.5,15.));
#20021=CARTESIAN_POINT('',(17.395,5.5,15.));
#20022=CARTESIAN_POINT('',(17.395,4.4,15.));
#20023=CARTESIAN_POINT('Origin',(18.,5.5,15.));
#20024=CARTESIAN_POINT('Origin',(21.2,7.8,0.9));
#20025=CARTESIAN_POINT('',(20.925,7.8,1.));
#20026=CARTESIAN_POINT('Origin',(21.2,7.8,1.));
#20027=CARTESIAN_POINT('',(20.925,7.8,1.8));
#20028=CARTESIAN_POINT('',(20.925,7.8,0.9));
#20029=CARTESIAN_POINT('Origin',(21.2,7.8,1.8));
#20030=CARTESIAN_POINT('Origin',(21.2,5.2,0.9));
#20031=CARTESIAN_POINT('',(20.925,5.2,1.));
#20032=CARTESIAN_POINT('Origin',(21.2,5.2,1.));
#20033=CARTESIAN_POINT('',(20.925,5.2,1.8));
#20034=CARTESIAN_POINT('',(20.925,5.2,0.9));
#20035=CARTESIAN_POINT('Origin',(21.2,5.2,1.8));
#20036=CARTESIAN_POINT('Origin',(14.8,7.8,0.9));
#20037=CARTESIAN_POINT('',(14.525,7.8,1.));
#20038=CARTESIAN_POINT('Origin',(14.8,7.8,1.));
#20039=CARTESIAN_POINT('',(14.525,7.8,1.8));
#20040=CARTESIAN_POINT('',(14.525,7.8,0.9));
#20041=CARTESIAN_POINT('Origin',(14.8,7.8,1.8));
#20042=CARTESIAN_POINT('Origin',(14.8,5.2,0.9));
#20043=CARTESIAN_POINT('',(14.525,5.2,1.));
#20044=CARTESIAN_POINT('Origin',(14.8,5.2,1.));
#20045=CARTESIAN_POINT('',(14.525,5.2,1.8));
#20046=CARTESIAN_POINT('',(14.525,5.2,0.9));
#20047=CARTESIAN_POINT('Origin',(14.8,5.2,1.8));
#20048=CARTESIAN_POINT('Origin',(14.,4.5,1.8));
#20049=CARTESIAN_POINT('',(15.5,5.5,1.8));
#20050=CARTESIAN_POINT('',(15.5,4.5,1.8));
#20051=CARTESIAN_POINT('',(15.5,5.,1.8));
#20052=CARTESIAN_POINT('',(20.5,5.5,1.8));
#20053=CARTESIAN_POINT('',(17.25,5.5,1.8));
#20054=CARTESIAN_POINT('',(20.5,4.5,1.8));
#20055=CARTESIAN_POINT('',(20.5,4.5,1.8));
#20056=CARTESIAN_POINT('',(22.,4.5,1.8));
#20057=CARTESIAN_POINT('',(22.,4.5,1.8));
#20058=CARTESIAN_POINT('',(22.,8.5,1.8));
#20059=CARTESIAN_POINT('',(22.,4.5,1.8));
#20060=CARTESIAN_POINT('',(14.,8.5,1.8));
#20061=CARTESIAN_POINT('',(22.,8.5,1.8));
#20062=CARTESIAN_POINT('',(14.,4.5,1.8));
#20063=CARTESIAN_POINT('',(14.,4.5,1.8));
#20064=CARTESIAN_POINT('',(22.,4.5,1.8));
#20065=CARTESIAN_POINT('Origin',(14.,4.5,1.));
#20066=CARTESIAN_POINT('',(14.,4.5,1.));
#20067=CARTESIAN_POINT('',(14.,4.5,1.8));
#20068=CARTESIAN_POINT('',(14.,8.5,1.));
#20069=CARTESIAN_POINT('',(14.,8.5,1.8));
#20070=CARTESIAN_POINT('',(14.,4.5,1.));
#20071=CARTESIAN_POINT('Origin',(22.,4.5,1.8));
#20072=CARTESIAN_POINT('',(22.,4.5,1.));
#20073=CARTESIAN_POINT('',(22.,4.5,1.));
#20074=CARTESIAN_POINT('',(22.,8.5,1.));
#20075=CARTESIAN_POINT('',(22.,4.5,1.));
#20076=CARTESIAN_POINT('',(22.,8.5,1.));
#20077=CARTESIAN_POINT('Origin',(18.,8.5,1.4));
#20078=CARTESIAN_POINT('',(14.,8.5,1.));
#20079=CARTESIAN_POINT('Origin',(15.5,4.5,1.));
#20080=CARTESIAN_POINT('',(20.5,4.5,18.));
#20081=CARTESIAN_POINT('',(20.5,4.5,1.));
#20082=CARTESIAN_POINT('',(15.5,4.5,18.));
#20083=CARTESIAN_POINT('',(15.5,4.5,18.));
#20084=CARTESIAN_POINT('',(15.5,4.5,1.));
#20085=CARTESIAN_POINT('',(14.,4.5,1.));
#20086=CARTESIAN_POINT('Origin',(20.5,4.5,1.));
#20087=CARTESIAN_POINT('',(20.5,5.5,18.));
#20088=CARTESIAN_POINT('',(20.5,5.5,1.));
#20089=CARTESIAN_POINT('',(20.5,4.5,18.));
#20090=CARTESIAN_POINT('Origin',(20.5,5.5,1.));
#20091=CARTESIAN_POINT('',(15.5,5.5,18.));
#20092=CARTESIAN_POINT('',(15.5,5.5,1.));
#20093=CARTESIAN_POINT('',(20.5,5.5,18.));
#20094=CARTESIAN_POINT('Origin',(15.5,5.5,1.));
#20095=CARTESIAN_POINT('',(15.5,5.5,18.));
#20096=CARTESIAN_POINT('Origin',(18.,5.,18.));
#20097=CARTESIAN_POINT('Origin',(18.,5.,1.));
#23501=UNCERTAINTY_MEASURE_WITH_UNIT(LENGTH_MEASURE(0.001),#23729,
'DISTANCE_ACCURACY_VALUE',
'Maximum model space distance between geometric entities at asserted c
onnectivities');
#23611=UNCERTAINTY_MEASURE_WITH_UNIT(LENGTH_MEASURE(0.001),#23729,
'DISTANCE_ACCURACY_VALUE',
'Maximum model space distance between geometric entities at asserted c
onnectivities');
#23618=(
GEOMETRIC_REPRESENTATION_CONTEXT(3)
GLOBAL_UNCERTAINTY_ASSIGNED_CONTEXT((#23501))
GLOBAL_UNIT_ASSIGNED_CONTEXT((#23729,#23731,#23732))
REPRESENTATION_CONTEXT('','3D')
);
#23728=(
GEOMETRIC_REPRESENTATION_CONTEXT(3)
GLOBAL_UNCERTAINTY_ASSIGNED_CONTEXT((#23611))
GLOBAL_UNIT_ASSIGNED_CONTEXT((#23729,#23731,#23732))
REPRESENTATION_CONTEXT('','3D')
);
#23729=(
LENGTH_UNIT()
NAMED_UNIT(*)
SI_UNIT(.CENTI.,.METRE.)
);
#23731=(
NAMED_UNIT(*)
PLANE_ANGLE_UNIT()
SI_UNIT($,.RADIAN.)
);
#23732=(
NAMED_UNIT(*)
SI_UNIT($,.STERADIAN.)
SOLID_ANGLE_UNIT()
);
#23739=SHAPE_DEFINITION_REPRESENTATION(#23855,#24118);
#23855=PRODUCT_DEFINITION_SHAPE('',$,#24235);
#24118=SHAPE_REPRESENTATION('',(#13770),#23618);
#24228=PRODUCT_DEFINITION_CONTEXT('part definition',#24578,'design');
#24235=PRODUCT_DEFINITION('Pivot post (1)','Pivot post (1)',#24351,#24228);
#24351=PRODUCT_DEFINITION_FORMATION('',$,#24586);
#24578=APPLICATION_CONTEXT(
'Core Data for Automotive Mechanical Design Process');
#24579=PRODUCT_CONTEXT('part definition',#24578,'mechanical');
#24586=PRODUCT('Pivot post (1)','Pivot post (1)','Pivot post (1)',(#24579));
#24773=COLOUR_RGB('Off White',0.89,0.88,0.83);
#24774=FILL_AREA_STYLE_COLOUR('',#24773);
#24775=FILL_AREA_STYLE('',(#24774));
#24776=SURFACE_STYLE_FILL_AREA(#24775);
#24777=SURFACE_SIDE_STYLE('',(#24776));
#24778=SURFACE_STYLE_USAGE(.BOTH.,#24777);
#24779=PRESENTATION_STYLE_ASSIGNMENT((#24778));
ENDSEC;
END-ISO-10303-21;
